ISO-10303-21;
HEADER;
/* Generated by software containing ST-Developer
 * from STEP Tools, Inc. (www.steptools.com) 
 */

FILE_DESCRIPTION(
/* description */ ('STEP AP214'),
/* implementation_level */ '2;1');

FILE_NAME(
/* name */ 'Hex Jam Nut 0.2500-20-D-S.step',
/* time_stamp */ '2026-11-14T04:30:00-08:00',
/* author */ (''),
/* organization */ (''),
/* preprocessor_version */ 'ST-DEVELOPER v20.2',
/* originating_system */ 'Autodesk Translation Framework v15.17.0.0',
/* authorisation */ '');

FILE_SCHEMA (('AUTOMOTIVE_DESIGN { 1 0 10303 214 3 1 1 }'));
ENDSEC;

DATA;
#10=MECHANICAL_DESIGN_GEOMETRIC_PRESENTATION_REPRESENTATION('',(#126),#40809);
#110=SHAPE_REPRESENTATION_RELATIONSHIP('SRR','None',#40860,#118);
#118=ADVANCED_BREP_SHAPE_REPRESENTATION('',(#134),#40804);
#126=STYLED_ITEM('',(#40909),#134);
#134=MANIFOLD_SOLID_BREP('Body1',#6301);
#213=(
BOUNDED_CURVE()
B_SPLINE_CURVE(2,(#39889,#39890,#39891),.UNSPECIFIED.,.F.,.F.)
B_SPLINE_CURVE_WITH_KNOTS((3,3),(0.700862393254458,1.2335087310839),
 .UNSPECIFIED.)
CURVE()
GEOMETRIC_REPRESENTATION_ITEM()
RATIONAL_B_SPLINE_CURVE((1.50938394797057,1.62613520265909,1.62613520265909))
REPRESENTATION_ITEM('')
);
#214=(
BOUNDED_CURVE()
B_SPLINE_CURVE(2,(#39893,#39894,#39895),.UNSPECIFIED.,.F.,.F.)
B_SPLINE_CURVE_WITH_KNOTS((3,3),(1.2335087310839,1.76615506891335),
 .UNSPECIFIED.)
CURVE()
GEOMETRIC_REPRESENTATION_ITEM()
RATIONAL_B_SPLINE_CURVE((1.62613520265909,1.62613520265909,1.50938394797057))
REPRESENTATION_ITEM('')
);
#215=(
BOUNDED_CURVE()
B_SPLINE_CURVE(2,(#39899,#39900,#39901),.UNSPECIFIED.,.F.,.F.)
B_SPLINE_CURVE_WITH_KNOTS((3,3),(-1.2335087310839,-0.70086239325445),
 .UNSPECIFIED.)
CURVE()
GEOMETRIC_REPRESENTATION_ITEM()
RATIONAL_B_SPLINE_CURVE((1.62613520265909,1.62613520265909,1.50938394797057))
REPRESENTATION_ITEM('')
);
#216=(
BOUNDED_CURVE()
B_SPLINE_CURVE(2,(#39902,#39903,#39904),.UNSPECIFIED.,.F.,.F.)
B_SPLINE_CURVE_WITH_KNOTS((3,3),(-1.76615506891334,-1.2335087310839),
 .UNSPECIFIED.)
CURVE()
GEOMETRIC_REPRESENTATION_ITEM()
RATIONAL_B_SPLINE_CURVE((1.50938394797057,1.62613520265909,1.62613520265909))
REPRESENTATION_ITEM('')
);
#217=(
BOUNDED_CURVE()
B_SPLINE_CURVE(2,(#39907,#39908,#39909),.UNSPECIFIED.,.F.,.F.)
B_SPLINE_CURVE_WITH_KNOTS((3,3),(0.700862393254451,1.2335087310839),
 .UNSPECIFIED.)
CURVE()
GEOMETRIC_REPRESENTATION_ITEM()
RATIONAL_B_SPLINE_CURVE((1.50938394797057,1.62613520265909,1.62613520265909))
REPRESENTATION_ITEM('')
);
#218=(
BOUNDED_CURVE()
B_SPLINE_CURVE(2,(#39911,#39912,#39913),.UNSPECIFIED.,.F.,.F.)
B_SPLINE_CURVE_WITH_KNOTS((3,3),(1.2335087310839,1.76615506891334),
 .UNSPECIFIED.)
CURVE()
GEOMETRIC_REPRESENTATION_ITEM()
RATIONAL_B_SPLINE_CURVE((1.62613520265909,1.62613520265909,1.50938394797057))
REPRESENTATION_ITEM('')
);
#219=(
BOUNDED_CURVE()
B_SPLINE_CURVE(2,(#39917,#39918,#39919),.UNSPECIFIED.,.F.,.F.)
B_SPLINE_CURVE_WITH_KNOTS((3,3),(-1.2335087310839,-0.700862393254457),
 .UNSPECIFIED.)
CURVE()
GEOMETRIC_REPRESENTATION_ITEM()
RATIONAL_B_SPLINE_CURVE((1.62613520265909,1.62613520265909,1.50938394797057))
REPRESENTATION_ITEM('')
);
#220=(
BOUNDED_CURVE()
B_SPLINE_CURVE(2,(#39920,#39921,#39922),.UNSPECIFIED.,.F.,.F.)
B_SPLINE_CURVE_WITH_KNOTS((3,3),(-1.76615506891334,-1.2335087310839),
 .UNSPECIFIED.)
CURVE()
GEOMETRIC_REPRESENTATION_ITEM()
RATIONAL_B_SPLINE_CURVE((1.50938394797057,1.62613520265909,1.62613520265909))
REPRESENTATION_ITEM('')
);
#221=(
BOUNDED_CURVE()
B_SPLINE_CURVE(2,(#39926,#39927,#39928),.UNSPECIFIED.,.F.,.F.)
B_SPLINE_CURVE_WITH_KNOTS((3,3),(0.700862393254448,1.2335087310839),
 .UNSPECIFIED.)
CURVE()
GEOMETRIC_REPRESENTATION_ITEM()
RATIONAL_B_SPLINE_CURVE((1.50938394797057,1.62613520265909,1.62613520265909))
REPRESENTATION_ITEM('')
);
#222=(
BOUNDED_CURVE()
B_SPLINE_CURVE(2,(#39932,#39933,#39934),.UNSPECIFIED.,.F.,.F.)
B_SPLINE_CURVE_WITH_KNOTS((3,3),(-1.76615506891334,-1.23350873108389),
 .UNSPECIFIED.)
CURVE()
GEOMETRIC_REPRESENTATION_ITEM()
RATIONAL_B_SPLINE_CURVE((1.50938394797057,1.62613520265909,1.62613520265909))
REPRESENTATION_ITEM('')
);
#223=(
BOUNDED_CURVE()
B_SPLINE_CURVE(2,(#39935,#39936,#39937),.UNSPECIFIED.,.F.,.F.)
B_SPLINE_CURVE_WITH_KNOTS((3,3),(-1.23350873108389,-0.70086239325445),
 .UNSPECIFIED.)
CURVE()
GEOMETRIC_REPRESENTATION_ITEM()
RATIONAL_B_SPLINE_CURVE((1.62613520265909,1.62613520265909,1.50938394797057))
REPRESENTATION_ITEM('')
);
#224=(
BOUNDED_CURVE()
B_SPLINE_CURVE(2,(#39938,#39939,#39940),.UNSPECIFIED.,.F.,.F.)
B_SPLINE_CURVE_WITH_KNOTS((3,3),(1.2335087310839,1.76615506891334),
 .UNSPECIFIED.)
CURVE()
GEOMETRIC_REPRESENTATION_ITEM()
RATIONAL_B_SPLINE_CURVE((1.62613520265909,1.62613520265909,1.50938394797057))
REPRESENTATION_ITEM('')
);
#225=(
BOUNDED_CURVE()
B_SPLINE_CURVE(2,(#39943,#39944,#39945),.UNSPECIFIED.,.F.,.F.)
B_SPLINE_CURVE_WITH_KNOTS((3,3),(0.700862393254458,1.23350873108389),
 .UNSPECIFIED.)
CURVE()
GEOMETRIC_REPRESENTATION_ITEM()
RATIONAL_B_SPLINE_CURVE((1.50938394797057,1.62613520265908,1.62613520265908))
REPRESENTATION_ITEM('')
);
#226=(
BOUNDED_CURVE()
B_SPLINE_CURVE(2,(#39947,#39948,#39949),.UNSPECIFIED.,.F.,.F.)
B_SPLINE_CURVE_WITH_KNOTS((3,3),(1.23350873108389,1.76615506891335),
 .UNSPECIFIED.)
CURVE()
GEOMETRIC_REPRESENTATION_ITEM()
RATIONAL_B_SPLINE_CURVE((1.62613520265908,1.62613520265908,1.50938394797056))
REPRESENTATION_ITEM('')
);
#227=(
BOUNDED_CURVE()
B_SPLINE_CURVE(2,(#39953,#39954,#39955),.UNSPECIFIED.,.F.,.F.)
B_SPLINE_CURVE_WITH_KNOTS((3,3),(-1.23350873108389,-0.700862393254442),
 .UNSPECIFIED.)
CURVE()
GEOMETRIC_REPRESENTATION_ITEM()
RATIONAL_B_SPLINE_CURVE((1.62613520265908,1.62613520265908,1.50938394797056))
REPRESENTATION_ITEM('')
);
#228=(
BOUNDED_CURVE()
B_SPLINE_CURVE(2,(#39956,#39957,#39958),.UNSPECIFIED.,.F.,.F.)
B_SPLINE_CURVE_WITH_KNOTS((3,3),(-1.76615506891333,-1.23350873108389),
 .UNSPECIFIED.)
CURVE()
GEOMETRIC_REPRESENTATION_ITEM()
RATIONAL_B_SPLINE_CURVE((1.50938394797057,1.62613520265908,1.62613520265908))
REPRESENTATION_ITEM('')
);
#229=(
BOUNDED_CURVE()
B_SPLINE_CURVE(2,(#39961,#39962,#39963),.UNSPECIFIED.,.F.,.F.)
B_SPLINE_CURVE_WITH_KNOTS((3,3),(0.700862393254457,1.23350873108389),
 .UNSPECIFIED.)
CURVE()
GEOMETRIC_REPRESENTATION_ITEM()
RATIONAL_B_SPLINE_CURVE((1.50938394797056,1.62613520265908,1.62613520265908))
REPRESENTATION_ITEM('')
);
#230=(
BOUNDED_CURVE()
B_SPLINE_CURVE(2,(#39965,#39966,#39967),.UNSPECIFIED.,.F.,.F.)
B_SPLINE_CURVE_WITH_KNOTS((3,3),(1.23350873108389,1.76615506891333),
 .UNSPECIFIED.)
CURVE()
GEOMETRIC_REPRESENTATION_ITEM()
RATIONAL_B_SPLINE_CURVE((1.62613520265908,1.62613520265908,1.50938394797056))
REPRESENTATION_ITEM('')
);
#231=(
BOUNDED_CURVE()
B_SPLINE_CURVE(2,(#39971,#39972,#39973),.UNSPECIFIED.,.F.,.F.)
B_SPLINE_CURVE_WITH_KNOTS((3,3),(-1.23350873108389,-0.700862393254458),
 .UNSPECIFIED.)
CURVE()
GEOMETRIC_REPRESENTATION_ITEM()
RATIONAL_B_SPLINE_CURVE((1.62613520265908,1.62613520265908,1.50938394797057))
REPRESENTATION_ITEM('')
);
#232=(
BOUNDED_CURVE()
B_SPLINE_CURVE(2,(#39974,#39975,#39976),.UNSPECIFIED.,.F.,.F.)
B_SPLINE_CURVE_WITH_KNOTS((3,3),(-1.76615506891333,-1.23350873108389),
 .UNSPECIFIED.)
CURVE()
GEOMETRIC_REPRESENTATION_ITEM()
RATIONAL_B_SPLINE_CURVE((1.50938394797056,1.62613520265908,1.62613520265908))
REPRESENTATION_ITEM('')
);
#233=(
BOUNDED_CURVE()
B_SPLINE_CURVE(2,(#39979,#39980,#39981),.UNSPECIFIED.,.F.,.F.)
B_SPLINE_CURVE_WITH_KNOTS((3,3),(0.700862393254449,1.2335087310839),
 .UNSPECIFIED.)
CURVE()
GEOMETRIC_REPRESENTATION_ITEM()
RATIONAL_B_SPLINE_CURVE((1.50938394797057,1.62613520265909,1.62613520265909))
REPRESENTATION_ITEM('')
);
#234=(
BOUNDED_CURVE()
B_SPLINE_CURVE(2,(#39982,#39983,#39984),.UNSPECIFIED.,.F.,.F.)
B_SPLINE_CURVE_WITH_KNOTS((3,3),(1.2335087310839,1.76615506891334),
 .UNSPECIFIED.)
CURVE()
GEOMETRIC_REPRESENTATION_ITEM()
RATIONAL_B_SPLINE_CURVE((1.62613520265909,1.62613520265909,1.50938394797057))
REPRESENTATION_ITEM('')
);
#235=(
BOUNDED_CURVE()
B_SPLINE_CURVE(2,(#39986,#39987,#39988),.UNSPECIFIED.,.F.,.F.)
B_SPLINE_CURVE_WITH_KNOTS((3,3),(-1.2335087310839,-0.700862393254449),
 .UNSPECIFIED.)
CURVE()
GEOMETRIC_REPRESENTATION_ITEM()
RATIONAL_B_SPLINE_CURVE((1.62613520265909,1.62613520265909,1.50938394797057))
REPRESENTATION_ITEM('')
);
#236=(
BOUNDED_CURVE()
B_SPLINE_CURVE(2,(#39989,#39990,#39991),.UNSPECIFIED.,.F.,.F.)
B_SPLINE_CURVE_WITH_KNOTS((3,3),(-1.76615506891334,-1.2335087310839),
 .UNSPECIFIED.)
CURVE()
GEOMETRIC_REPRESENTATION_ITEM()
RATIONAL_B_SPLINE_CURVE((1.50938394797057,1.62613520265909,1.62613520265909))
REPRESENTATION_ITEM('')
);
#288=PLANE('',#6796);
#289=PLANE('',#6797);
#290=PLANE('',#6798);
#291=PLANE('',#6799);
#292=PLANE('',#6800);
#293=PLANE('',#6801);
#294=PLANE('',#6802);
#295=PLANE('',#6809);
#351=FACE_BOUND('',#1128,.T.);
#352=FACE_BOUND('',#1130,.T.);
#385=CONICAL_SURFACE('',#6755,2.5527,0.959931088596876);
#386=CONICAL_SURFACE('',#6759,3.175,0.959931088596891);
#387=CONICAL_SURFACE('',#6762,2.5527,0.959931088596876);
#388=CONICAL_SURFACE('',#6766,3.175,0.959931088596891);
#389=CONICAL_SURFACE('',#6769,2.5527,0.959931088596876);
#390=CONICAL_SURFACE('',#6773,3.175,0.959931088596891);
#391=CONICAL_SURFACE('',#6776,2.5527,0.959931088596876);
#392=CONICAL_SURFACE('',#6780,3.175,0.959931088596891);
#393=CONICAL_SURFACE('',#6787,3.175,0.95993108859688);
#394=CONICAL_SURFACE('',#6790,2.49047,0.959931088596878);
#395=CONICAL_SURFACE('',#6816,5.55625,0.934531290657969);
#396=CONICAL_SURFACE('',#6817,5.55625,0.934531290657969);
#397=CONICAL_SURFACE('',#6818,5.55625,0.934531290657969);
#398=CONICAL_SURFACE('',#6819,5.55625,0.934531290657969);
#399=CONICAL_SURFACE('',#6820,5.55625,0.934531290657969);
#400=CONICAL_SURFACE('',#6821,5.55625,0.934531290657969);
#401=CONICAL_SURFACE('',#6822,5.55625,0.934531290657969);
#402=CONICAL_SURFACE('',#6823,5.55625,0.934531290657969);
#403=CONICAL_SURFACE('',#6824,5.55625,0.934531290657969);
#404=CONICAL_SURFACE('',#6825,5.55625,0.934531290657969);
#405=CONICAL_SURFACE('',#6826,5.55625,0.934531290657969);
#406=CONICAL_SURFACE('',#6827,5.55625,0.934531290657969);
#707=FACE_OUTER_BOUND('',#1106,.T.);
#708=FACE_OUTER_BOUND('',#1107,.T.);
#709=FACE_OUTER_BOUND('',#1108,.T.);
#710=FACE_OUTER_BOUND('',#1109,.T.);
#711=FACE_OUTER_BOUND('',#1110,.T.);
#712=FACE_OUTER_BOUND('',#1111,.T.);
#713=FACE_OUTER_BOUND('',#1112,.T.);
#714=FACE_OUTER_BOUND('',#1113,.T.);
#715=FACE_OUTER_BOUND('',#1114,.T.);
#716=FACE_OUTER_BOUND('',#1115,.T.);
#717=FACE_OUTER_BOUND('',#1116,.T.);
#718=FACE_OUTER_BOUND('',#1117,.T.);
#719=FACE_OUTER_BOUND('',#1118,.T.);
#720=FACE_OUTER_BOUND('',#1119,.T.);
#721=FACE_OUTER_BOUND('',#1120,.T.);
#722=FACE_OUTER_BOUND('',#1121,.T.);
#723=FACE_OUTER_BOUND('',#1122,.T.);
#724=FACE_OUTER_BOUND('',#1123,.T.);
#725=FACE_OUTER_BOUND('',#1124,.T.);
#726=FACE_OUTER_BOUND('',#1125,.T.);
#727=FACE_OUTER_BOUND('',#1126,.T.);
#728=FACE_OUTER_BOUND('',#1127,.T.);
#729=FACE_OUTER_BOUND('',#1129,.T.);
#730=FACE_OUTER_BOUND('',#1131,.T.);
#731=FACE_OUTER_BOUND('',#1132,.T.);
#732=FACE_OUTER_BOUND('',#1133,.T.);
#733=FACE_OUTER_BOUND('',#1134,.T.);
#734=FACE_OUTER_BOUND('',#1135,.T.);
#735=FACE_OUTER_BOUND('',#1136,.T.);
#736=FACE_OUTER_BOUND('',#1137,.T.);
#737=FACE_OUTER_BOUND('',#1138,.T.);
#738=FACE_OUTER_BOUND('',#1139,.T.);
#739=FACE_OUTER_BOUND('',#1140,.T.);
#740=FACE_OUTER_BOUND('',#1141,.T.);
#741=FACE_OUTER_BOUND('',#1142,.T.);
#1106=EDGE_LOOP('',(#4934,#4935,#4936,#4937,#4938));
#1107=EDGE_LOOP('',(#4939,#4940,#4941,#4942,#4943,#4944));
#1108=EDGE_LOOP('',(#4945,#4946,#4947,#4948,#4949));
#1109=EDGE_LOOP('',(#4950,#4951,#4952,#4953,#4954,#4955));
#1110=EDGE_LOOP('',(#4956,#4957,#4958,#4959,#4960));
#1111=EDGE_LOOP('',(#4961,#4962,#4963,#4964,#4965,#4966));
#1112=EDGE_LOOP('',(#4967,#4968,#4969,#4970,#4971));
#1113=EDGE_LOOP('',(#4972,#4973,#4974,#4975,#4976,#4977));
#1114=EDGE_LOOP('',(#4978,#4979,#4980,#4981,#4982));
#1115=EDGE_LOOP('',(#4983,#4984,#4985,#4986,#4987,#4988));
#1116=EDGE_LOOP('',(#4989,#4990,#4991,#4992,#4993));
#1117=EDGE_LOOP('',(#4994,#4995,#4996,#4997,#4998));
#1118=EDGE_LOOP('',(#4999,#5000,#5001,#5002,#5003));
#1119=EDGE_LOOP('',(#5004,#5005,#5006,#5007,#5008));
#1120=EDGE_LOOP('',(#5009,#5010,#5011,#5012,#5013));
#1121=EDGE_LOOP('',(#5014,#5015,#5016,#5017,#5018,#5019));
#1122=EDGE_LOOP('',(#5020,#5021,#5022,#5023,#5024,#5025));
#1123=EDGE_LOOP('',(#5026,#5027,#5028,#5029,#5030,#5031));
#1124=EDGE_LOOP('',(#5032,#5033,#5034,#5035,#5036,#5037));
#1125=EDGE_LOOP('',(#5038,#5039,#5040,#5041,#5042,#5043));
#1126=EDGE_LOOP('',(#5044,#5045,#5046,#5047,#5048,#5049));
#1127=EDGE_LOOP('',(#5050,#5051,#5052,#5053,#5054,#5055));
#1128=EDGE_LOOP('',(#5056));
#1129=EDGE_LOOP('',(#5057,#5058,#5059,#5060,#5061,#5062));
#1130=EDGE_LOOP('',(#5063));
#1131=EDGE_LOOP('',(#5064,#5065,#5066));
#1132=EDGE_LOOP('',(#5067,#5068,#5069));
#1133=EDGE_LOOP('',(#5070,#5071,#5072));
#1134=EDGE_LOOP('',(#5073,#5074,#5075));
#1135=EDGE_LOOP('',(#5076,#5077,#5078));
#1136=EDGE_LOOP('',(#5079,#5080,#5081));
#1137=EDGE_LOOP('',(#5082,#5083,#5084));
#1138=EDGE_LOOP('',(#5085,#5086,#5087));
#1139=EDGE_LOOP('',(#5088,#5089,#5090));
#1140=EDGE_LOOP('',(#5091,#5092,#5093));
#1141=EDGE_LOOP('',(#5094,#5095,#5096));
#1142=EDGE_LOOP('',(#5097,#5098,#5099));
#1474=CIRCLE('',#6756,2.5527);
#1475=CIRCLE('',#6757,3.175);
#1476=CIRCLE('',#6758,3.175);
#1477=CIRCLE('',#6760,2.5527);
#1478=CIRCLE('',#6761,2.5527);
#1479=CIRCLE('',#6763,2.5527);
#1480=CIRCLE('',#6764,3.175);
#1481=CIRCLE('',#6765,3.175);
#1482=CIRCLE('',#6767,2.5527);
#1483=CIRCLE('',#6768,2.5527);
#1484=CIRCLE('',#6770,2.5527);
#1485=CIRCLE('',#6771,3.175);
#1486=CIRCLE('',#6772,3.175);
#1487=CIRCLE('',#6774,2.5527);
#1488=CIRCLE('',#6775,2.5527);
#1489=CIRCLE('',#6777,2.5527);
#1490=CIRCLE('',#6778,3.175);
#1491=CIRCLE('',#6779,3.175);
#1492=CIRCLE('',#6781,3.15686252031437);
#1493=CIRCLE('',#6782,3.15686252031437);
#1494=CIRCLE('',#6784,3.175);
#1495=CIRCLE('',#6785,3.175);
#1496=CIRCLE('',#6786,3.175);
#1497=CIRCLE('',#6788,2.5527);
#1498=CIRCLE('',#6789,2.5527);
#1499=CIRCLE('',#6791,3.175);
#1500=CIRCLE('',#6803,5.55625);
#1501=CIRCLE('',#6804,5.55625);
#1502=CIRCLE('',#6805,5.55625);
#1503=CIRCLE('',#6806,5.55625);
#1504=CIRCLE('',#6807,5.55625);
#1505=CIRCLE('',#6808,5.55625);
#1506=CIRCLE('',#6810,5.55625);
#1507=CIRCLE('',#6811,5.55625);
#1508=CIRCLE('',#6812,5.55625);
#1509=CIRCLE('',#6813,5.55625);
#1510=CIRCLE('',#6814,5.55625);
#1511=CIRCLE('',#6815,5.55625);
#1984=LINE('',#39806,#2302);
#1985=LINE('',#39815,#2303);
#1986=LINE('',#39820,#2304);
#1987=LINE('',#39829,#2305);
#1988=LINE('',#39834,#2306);
#1989=LINE('',#39843,#2307);
#1990=LINE('',#39848,#2308);
#1991=LINE('',#39856,#2309);
#1992=LINE('',#39862,#2310);
#1993=LINE('',#39870,#2311);
#1994=LINE('',#39874,#2312);
#1995=LINE('',#39877,#2313);
#1996=LINE('',#39879,#2314);
#1997=LINE('',#39881,#2315);
#1998=LINE('',#39883,#2316);
#1999=LINE('',#39887,#2317);
#2000=LINE('',#39897,#2318);
#2001=LINE('',#39915,#2319);
#2002=LINE('',#39930,#2320);
#2003=LINE('',#39951,#2321);
#2004=LINE('',#39969,#2322);
#2302=VECTOR('',#8066,2.5527);
#2303=VECTOR('',#8077,3.175);
#2304=VECTOR('',#8082,2.5527);
#2305=VECTOR('',#8093,3.175);
#2306=VECTOR('',#8098,2.5527);
#2307=VECTOR('',#8109,3.175);
#2308=VECTOR('',#8114,2.5527);
#2309=VECTOR('',#8123,3.175);
#2310=VECTOR('',#8130,3.175);
#2311=VECTOR('',#8139,3.175);
#2312=VECTOR('',#8144,2.49047);
#2313=VECTOR('',#8149,2.5527);
#2314=VECTOR('',#8152,2.5527);
#2315=VECTOR('',#8155,2.5527);
#2316=VECTOR('',#8158,2.5527);
#2317=VECTOR('',#8161,1000.);
#2318=VECTOR('',#8162,1000.);
#2319=VECTOR('',#8165,1000.);
#2320=VECTOR('',#8168,1000.);
#2321=VECTOR('',#8171,1000.);
#2322=VECTOR('',#8174,1000.);
#2763=VERTEX_POINT('',#39803);
#2764=VERTEX_POINT('',#39805);
#2765=VERTEX_POINT('',#39807);
#2766=VERTEX_POINT('',#39811);
#2767=VERTEX_POINT('',#39812);
#2768=VERTEX_POINT('',#39817);
#2769=VERTEX_POINT('',#39819);
#2770=VERTEX_POINT('',#39821);
#2771=VERTEX_POINT('',#39825);
#2772=VERTEX_POINT('',#39826);
#2773=VERTEX_POINT('',#39831);
#2774=VERTEX_POINT('',#39833);
#2775=VERTEX_POINT('',#39835);
#2776=VERTEX_POINT('',#39839);
#2777=VERTEX_POINT('',#39840);
#2778=VERTEX_POINT('',#39845);
#2779=VERTEX_POINT('',#39847);
#2780=VERTEX_POINT('',#39849);
#2781=VERTEX_POINT('',#39853);
#2782=VERTEX_POINT('',#39854);
#2783=VERTEX_POINT('',#39859);
#2784=VERTEX_POINT('',#39861);
#2785=VERTEX_POINT('',#39863);
#2786=VERTEX_POINT('',#39867);
#2787=VERTEX_POINT('',#39868);
#2788=VERTEX_POINT('',#39873);
#2789=VERTEX_POINT('',#39885);
#2790=VERTEX_POINT('',#39886);
#2791=VERTEX_POINT('',#39888);
#2792=VERTEX_POINT('',#39892);
#2793=VERTEX_POINT('',#39896);
#2794=VERTEX_POINT('',#39898);
#2795=VERTEX_POINT('',#39906);
#2796=VERTEX_POINT('',#39910);
#2797=VERTEX_POINT('',#39914);
#2798=VERTEX_POINT('',#39916);
#2799=VERTEX_POINT('',#39924);
#2800=VERTEX_POINT('',#39925);
#2801=VERTEX_POINT('',#39929);
#2802=VERTEX_POINT('',#39931);
#2803=VERTEX_POINT('',#39942);
#2804=VERTEX_POINT('',#39946);
#2805=VERTEX_POINT('',#39950);
#2806=VERTEX_POINT('',#39952);
#2807=VERTEX_POINT('',#39960);
#2808=VERTEX_POINT('',#39964);
#2809=VERTEX_POINT('',#39968);
#2810=VERTEX_POINT('',#39970);
#2811=VERTEX_POINT('',#39978);
#2812=VERTEX_POINT('',#39985);
#3519=EDGE_CURVE('',#2763,#2763,#1474,.T.);
#3520=EDGE_CURVE('',#2763,#2764,#1984,.T.);
#3521=EDGE_CURVE('',#2765,#2764,#1475,.T.);
#3522=EDGE_CURVE('',#2764,#2765,#1476,.T.);
#3523=EDGE_CURVE('',#2766,#2767,#1477,.T.);
#3524=EDGE_CURVE('',#2767,#2766,#1478,.T.);
#3525=EDGE_CURVE('',#2767,#2765,#1985,.T.);
#3526=EDGE_CURVE('',#2768,#2768,#1479,.T.);
#3527=EDGE_CURVE('',#2768,#2769,#1986,.T.);
#3528=EDGE_CURVE('',#2770,#2769,#1480,.T.);
#3529=EDGE_CURVE('',#2769,#2770,#1481,.T.);
#3530=EDGE_CURVE('',#2771,#2772,#1482,.T.);
#3531=EDGE_CURVE('',#2772,#2771,#1483,.T.);
#3532=EDGE_CURVE('',#2772,#2770,#1987,.T.);
#3533=EDGE_CURVE('',#2773,#2773,#1484,.T.);
#3534=EDGE_CURVE('',#2773,#2774,#1988,.T.);
#3535=EDGE_CURVE('',#2775,#2774,#1485,.T.);
#3536=EDGE_CURVE('',#2774,#2775,#1486,.T.);
#3537=EDGE_CURVE('',#2776,#2777,#1487,.T.);
#3538=EDGE_CURVE('',#2777,#2776,#1488,.T.);
#3539=EDGE_CURVE('',#2777,#2775,#1989,.T.);
#3540=EDGE_CURVE('',#2778,#2778,#1489,.T.);
#3541=EDGE_CURVE('',#2778,#2779,#1990,.T.);
#3542=EDGE_CURVE('',#2780,#2779,#1490,.T.);
#3543=EDGE_CURVE('',#2779,#2780,#1491,.T.);
#3544=EDGE_CURVE('',#2781,#2782,#1492,.T.);
#3545=EDGE_CURVE('',#2782,#2780,#1991,.T.);
#3546=EDGE_CURVE('',#2782,#2781,#1493,.T.);
#3547=EDGE_CURVE('',#2783,#2783,#1494,.T.);
#3548=EDGE_CURVE('',#2783,#2784,#1992,.T.);
#3549=EDGE_CURVE('',#2784,#2785,#1495,.T.);
#3550=EDGE_CURVE('',#2785,#2784,#1496,.T.);
#3551=EDGE_CURVE('',#2786,#2787,#1497,.T.);
#3552=EDGE_CURVE('',#2787,#2785,#1993,.T.);
#3553=EDGE_CURVE('',#2787,#2786,#1498,.T.);
#3554=EDGE_CURVE('',#2781,#2788,#1994,.T.);
#3555=EDGE_CURVE('',#2788,#2788,#1499,.T.);
#3556=EDGE_CURVE('',#2776,#2778,#1995,.T.);
#3557=EDGE_CURVE('',#2771,#2773,#1996,.T.);
#3558=EDGE_CURVE('',#2766,#2768,#1997,.T.);
#3559=EDGE_CURVE('',#2786,#2763,#1998,.T.);
#3560=EDGE_CURVE('',#2789,#2790,#1999,.T.);
#3561=EDGE_CURVE('',#2790,#2791,#213,.T.);
#3562=EDGE_CURVE('',#2791,#2792,#214,.T.);
#3563=EDGE_CURVE('',#2793,#2792,#2000,.T.);
#3564=EDGE_CURVE('',#2794,#2793,#215,.T.);
#3565=EDGE_CURVE('',#2789,#2794,#216,.T.);
#3566=EDGE_CURVE('',#2792,#2795,#217,.T.);
#3567=EDGE_CURVE('',#2795,#2796,#218,.T.);
#3568=EDGE_CURVE('',#2797,#2796,#2001,.T.);
#3569=EDGE_CURVE('',#2798,#2797,#219,.T.);
#3570=EDGE_CURVE('',#2793,#2798,#220,.T.);
#3571=EDGE_CURVE('',#2799,#2800,#221,.T.);
#3572=EDGE_CURVE('',#2801,#2799,#2002,.T.);
#3573=EDGE_CURVE('',#2801,#2802,#222,.T.);
#3574=EDGE_CURVE('',#2802,#2797,#223,.T.);
#3575=EDGE_CURVE('',#2800,#2796,#224,.T.);
#3576=EDGE_CURVE('',#2799,#2803,#225,.T.);
#3577=EDGE_CURVE('',#2803,#2804,#226,.T.);
#3578=EDGE_CURVE('',#2805,#2804,#2003,.T.);
#3579=EDGE_CURVE('',#2806,#2805,#227,.T.);
#3580=EDGE_CURVE('',#2801,#2806,#228,.T.);
#3581=EDGE_CURVE('',#2804,#2807,#229,.T.);
#3582=EDGE_CURVE('',#2807,#2808,#230,.T.);
#3583=EDGE_CURVE('',#2809,#2808,#2004,.T.);
#3584=EDGE_CURVE('',#2810,#2809,#231,.T.);
#3585=EDGE_CURVE('',#2805,#2810,#232,.T.);
#3586=EDGE_CURVE('',#2808,#2811,#233,.T.);
#3587=EDGE_CURVE('',#2811,#2790,#234,.T.);
#3588=EDGE_CURVE('',#2812,#2789,#235,.T.);
#3589=EDGE_CURVE('',#2809,#2812,#236,.T.);
#3590=EDGE_CURVE('',#2803,#2800,#1500,.T.);
#3591=EDGE_CURVE('',#2800,#2795,#1501,.T.);
#3592=EDGE_CURVE('',#2795,#2791,#1502,.T.);
#3593=EDGE_CURVE('',#2791,#2811,#1503,.T.);
#3594=EDGE_CURVE('',#2811,#2807,#1504,.T.);
#3595=EDGE_CURVE('',#2807,#2803,#1505,.T.);
#3596=EDGE_CURVE('',#2802,#2798,#1506,.T.);
#3597=EDGE_CURVE('',#2802,#2806,#1507,.T.);
#3598=EDGE_CURVE('',#2806,#2810,#1508,.T.);
#3599=EDGE_CURVE('',#2810,#2812,#1509,.T.);
#3600=EDGE_CURVE('',#2812,#2794,#1510,.T.);
#3601=EDGE_CURVE('',#2794,#2798,#1511,.T.);
#4934=ORIENTED_EDGE('',*,*,#3519,.T.);
#4935=ORIENTED_EDGE('',*,*,#3520,.T.);
#4936=ORIENTED_EDGE('',*,*,#3521,.F.);
#4937=ORIENTED_EDGE('',*,*,#3522,.F.);
#4938=ORIENTED_EDGE('',*,*,#3520,.F.);
#4939=ORIENTED_EDGE('',*,*,#3523,.F.);
#4940=ORIENTED_EDGE('',*,*,#3524,.F.);
#4941=ORIENTED_EDGE('',*,*,#3525,.T.);
#4942=ORIENTED_EDGE('',*,*,#3521,.T.);
#4943=ORIENTED_EDGE('',*,*,#3522,.T.);
#4944=ORIENTED_EDGE('',*,*,#3525,.F.);
#4945=ORIENTED_EDGE('',*,*,#3526,.T.);
#4946=ORIENTED_EDGE('',*,*,#3527,.T.);
#4947=ORIENTED_EDGE('',*,*,#3528,.F.);
#4948=ORIENTED_EDGE('',*,*,#3529,.F.);
#4949=ORIENTED_EDGE('',*,*,#3527,.F.);
#4950=ORIENTED_EDGE('',*,*,#3530,.F.);
#4951=ORIENTED_EDGE('',*,*,#3531,.F.);
#4952=ORIENTED_EDGE('',*,*,#3532,.T.);
#4953=ORIENTED_EDGE('',*,*,#3528,.T.);
#4954=ORIENTED_EDGE('',*,*,#3529,.T.);
#4955=ORIENTED_EDGE('',*,*,#3532,.F.);
#4956=ORIENTED_EDGE('',*,*,#3533,.T.);
#4957=ORIENTED_EDGE('',*,*,#3534,.T.);
#4958=ORIENTED_EDGE('',*,*,#3535,.F.);
#4959=ORIENTED_EDGE('',*,*,#3536,.F.);
#4960=ORIENTED_EDGE('',*,*,#3534,.F.);
#4961=ORIENTED_EDGE('',*,*,#3537,.F.);
#4962=ORIENTED_EDGE('',*,*,#3538,.F.);
#4963=ORIENTED_EDGE('',*,*,#3539,.T.);
#4964=ORIENTED_EDGE('',*,*,#3535,.T.);
#4965=ORIENTED_EDGE('',*,*,#3536,.T.);
#4966=ORIENTED_EDGE('',*,*,#3539,.F.);
#4967=ORIENTED_EDGE('',*,*,#3540,.T.);
#4968=ORIENTED_EDGE('',*,*,#3541,.T.);
#4969=ORIENTED_EDGE('',*,*,#3542,.F.);
#4970=ORIENTED_EDGE('',*,*,#3543,.F.);
#4971=ORIENTED_EDGE('',*,*,#3541,.F.);
#4972=ORIENTED_EDGE('',*,*,#3544,.T.);
#4973=ORIENTED_EDGE('',*,*,#3545,.T.);
#4974=ORIENTED_EDGE('',*,*,#3542,.T.);
#4975=ORIENTED_EDGE('',*,*,#3543,.T.);
#4976=ORIENTED_EDGE('',*,*,#3545,.F.);
#4977=ORIENTED_EDGE('',*,*,#3546,.T.);
#4978=ORIENTED_EDGE('',*,*,#3547,.T.);
#4979=ORIENTED_EDGE('',*,*,#3548,.T.);
#4980=ORIENTED_EDGE('',*,*,#3549,.T.);
#4981=ORIENTED_EDGE('',*,*,#3550,.T.);
#4982=ORIENTED_EDGE('',*,*,#3548,.F.);
#4983=ORIENTED_EDGE('',*,*,#3551,.T.);
#4984=ORIENTED_EDGE('',*,*,#3552,.T.);
#4985=ORIENTED_EDGE('',*,*,#3549,.F.);
#4986=ORIENTED_EDGE('',*,*,#3550,.F.);
#4987=ORIENTED_EDGE('',*,*,#3552,.F.);
#4988=ORIENTED_EDGE('',*,*,#3553,.T.);
#4989=ORIENTED_EDGE('',*,*,#3544,.F.);
#4990=ORIENTED_EDGE('',*,*,#3554,.T.);
#4991=ORIENTED_EDGE('',*,*,#3555,.T.);
#4992=ORIENTED_EDGE('',*,*,#3554,.F.);
#4993=ORIENTED_EDGE('',*,*,#3546,.F.);
#4994=ORIENTED_EDGE('',*,*,#3537,.T.);
#4995=ORIENTED_EDGE('',*,*,#3538,.T.);
#4996=ORIENTED_EDGE('',*,*,#3556,.T.);
#4997=ORIENTED_EDGE('',*,*,#3540,.F.);
#4998=ORIENTED_EDGE('',*,*,#3556,.F.);
#4999=ORIENTED_EDGE('',*,*,#3530,.T.);
#5000=ORIENTED_EDGE('',*,*,#3531,.T.);
#5001=ORIENTED_EDGE('',*,*,#3557,.T.);
#5002=ORIENTED_EDGE('',*,*,#3533,.F.);
#5003=ORIENTED_EDGE('',*,*,#3557,.F.);
#5004=ORIENTED_EDGE('',*,*,#3523,.T.);
#5005=ORIENTED_EDGE('',*,*,#3524,.T.);
#5006=ORIENTED_EDGE('',*,*,#3558,.T.);
#5007=ORIENTED_EDGE('',*,*,#3526,.F.);
#5008=ORIENTED_EDGE('',*,*,#3558,.F.);
#5009=ORIENTED_EDGE('',*,*,#3551,.F.);
#5010=ORIENTED_EDGE('',*,*,#3559,.T.);
#5011=ORIENTED_EDGE('',*,*,#3519,.F.);
#5012=ORIENTED_EDGE('',*,*,#3559,.F.);
#5013=ORIENTED_EDGE('',*,*,#3553,.F.);
#5014=ORIENTED_EDGE('',*,*,#3560,.T.);
#5015=ORIENTED_EDGE('',*,*,#3561,.T.);
#5016=ORIENTED_EDGE('',*,*,#3562,.T.);
#5017=ORIENTED_EDGE('',*,*,#3563,.F.);
#5018=ORIENTED_EDGE('',*,*,#3564,.F.);
#5019=ORIENTED_EDGE('',*,*,#3565,.F.);
#5020=ORIENTED_EDGE('',*,*,#3563,.T.);
#5021=ORIENTED_EDGE('',*,*,#3566,.T.);
#5022=ORIENTED_EDGE('',*,*,#3567,.T.);
#5023=ORIENTED_EDGE('',*,*,#3568,.F.);
#5024=ORIENTED_EDGE('',*,*,#3569,.F.);
#5025=ORIENTED_EDGE('',*,*,#3570,.F.);
#5026=ORIENTED_EDGE('',*,*,#3571,.F.);
#5027=ORIENTED_EDGE('',*,*,#3572,.F.);
#5028=ORIENTED_EDGE('',*,*,#3573,.T.);
#5029=ORIENTED_EDGE('',*,*,#3574,.T.);
#5030=ORIENTED_EDGE('',*,*,#3568,.T.);
#5031=ORIENTED_EDGE('',*,*,#3575,.F.);
#5032=ORIENTED_EDGE('',*,*,#3572,.T.);
#5033=ORIENTED_EDGE('',*,*,#3576,.T.);
#5034=ORIENTED_EDGE('',*,*,#3577,.T.);
#5035=ORIENTED_EDGE('',*,*,#3578,.F.);
#5036=ORIENTED_EDGE('',*,*,#3579,.F.);
#5037=ORIENTED_EDGE('',*,*,#3580,.F.);
#5038=ORIENTED_EDGE('',*,*,#3578,.T.);
#5039=ORIENTED_EDGE('',*,*,#3581,.T.);
#5040=ORIENTED_EDGE('',*,*,#3582,.T.);
#5041=ORIENTED_EDGE('',*,*,#3583,.F.);
#5042=ORIENTED_EDGE('',*,*,#3584,.F.);
#5043=ORIENTED_EDGE('',*,*,#3585,.F.);
#5044=ORIENTED_EDGE('',*,*,#3583,.T.);
#5045=ORIENTED_EDGE('',*,*,#3586,.T.);
#5046=ORIENTED_EDGE('',*,*,#3587,.T.);
#5047=ORIENTED_EDGE('',*,*,#3560,.F.);
#5048=ORIENTED_EDGE('',*,*,#3588,.F.);
#5049=ORIENTED_EDGE('',*,*,#3589,.F.);
#5050=ORIENTED_EDGE('',*,*,#3590,.T.);
#5051=ORIENTED_EDGE('',*,*,#3591,.T.);
#5052=ORIENTED_EDGE('',*,*,#3592,.T.);
#5053=ORIENTED_EDGE('',*,*,#3593,.T.);
#5054=ORIENTED_EDGE('',*,*,#3594,.T.);
#5055=ORIENTED_EDGE('',*,*,#3595,.T.);
#5056=ORIENTED_EDGE('',*,*,#3555,.F.);
#5057=ORIENTED_EDGE('',*,*,#3596,.F.);
#5058=ORIENTED_EDGE('',*,*,#3597,.T.);
#5059=ORIENTED_EDGE('',*,*,#3598,.T.);
#5060=ORIENTED_EDGE('',*,*,#3599,.T.);
#5061=ORIENTED_EDGE('',*,*,#3600,.T.);
#5062=ORIENTED_EDGE('',*,*,#3601,.T.);
#5063=ORIENTED_EDGE('',*,*,#3547,.F.);
#5064=ORIENTED_EDGE('',*,*,#3569,.T.);
#5065=ORIENTED_EDGE('',*,*,#3574,.F.);
#5066=ORIENTED_EDGE('',*,*,#3596,.T.);
#5067=ORIENTED_EDGE('',*,*,#3564,.T.);
#5068=ORIENTED_EDGE('',*,*,#3570,.T.);
#5069=ORIENTED_EDGE('',*,*,#3601,.F.);
#5070=ORIENTED_EDGE('',*,*,#3565,.T.);
#5071=ORIENTED_EDGE('',*,*,#3600,.F.);
#5072=ORIENTED_EDGE('',*,*,#3588,.T.);
#5073=ORIENTED_EDGE('',*,*,#3584,.T.);
#5074=ORIENTED_EDGE('',*,*,#3589,.T.);
#5075=ORIENTED_EDGE('',*,*,#3599,.F.);
#5076=ORIENTED_EDGE('',*,*,#3579,.T.);
#5077=ORIENTED_EDGE('',*,*,#3585,.T.);
#5078=ORIENTED_EDGE('',*,*,#3598,.F.);
#5079=ORIENTED_EDGE('',*,*,#3580,.T.);
#5080=ORIENTED_EDGE('',*,*,#3597,.F.);
#5081=ORIENTED_EDGE('',*,*,#3573,.F.);
#5082=ORIENTED_EDGE('',*,*,#3571,.T.);
#5083=ORIENTED_EDGE('',*,*,#3590,.F.);
#5084=ORIENTED_EDGE('',*,*,#3576,.F.);
#5085=ORIENTED_EDGE('',*,*,#3595,.F.);
#5086=ORIENTED_EDGE('',*,*,#3581,.F.);
#5087=ORIENTED_EDGE('',*,*,#3577,.F.);
#5088=ORIENTED_EDGE('',*,*,#3594,.F.);
#5089=ORIENTED_EDGE('',*,*,#3586,.F.);
#5090=ORIENTED_EDGE('',*,*,#3582,.F.);
#5091=ORIENTED_EDGE('',*,*,#3587,.F.);
#5092=ORIENTED_EDGE('',*,*,#3593,.F.);
#5093=ORIENTED_EDGE('',*,*,#3561,.F.);
#5094=ORIENTED_EDGE('',*,*,#3592,.F.);
#5095=ORIENTED_EDGE('',*,*,#3566,.F.);
#5096=ORIENTED_EDGE('',*,*,#3562,.F.);
#5097=ORIENTED_EDGE('',*,*,#3591,.F.);
#5098=ORIENTED_EDGE('',*,*,#3575,.T.);
#5099=ORIENTED_EDGE('',*,*,#3567,.F.);
#5867=CYLINDRICAL_SURFACE('',#6783,3.175);
#5868=CYLINDRICAL_SURFACE('',#6792,2.5527);
#5869=CYLINDRICAL_SURFACE('',#6793,2.5527);
#5870=CYLINDRICAL_SURFACE('',#6794,2.5527);
#5871=CYLINDRICAL_SURFACE('',#6795,2.5527);
#6122=ADVANCED_FACE('',(#707),#385,.F.);
#6123=ADVANCED_FACE('',(#708),#386,.F.);
#6124=ADVANCED_FACE('',(#709),#387,.F.);
#6125=ADVANCED_FACE('',(#710),#388,.F.);
#6126=ADVANCED_FACE('',(#711),#389,.F.);
#6127=ADVANCED_FACE('',(#712),#390,.F.);
#6128=ADVANCED_FACE('',(#713),#391,.F.);
#6129=ADVANCED_FACE('',(#714),#392,.F.);
#6130=ADVANCED_FACE('',(#715),#5867,.F.);
#6131=ADVANCED_FACE('',(#716),#393,.F.);
#6132=ADVANCED_FACE('',(#717),#394,.F.);
#6133=ADVANCED_FACE('',(#718),#5868,.F.);
#6134=ADVANCED_FACE('',(#719),#5869,.F.);
#6135=ADVANCED_FACE('',(#720),#5870,.F.);
#6136=ADVANCED_FACE('',(#721),#5871,.F.);
#6137=ADVANCED_FACE('',(#722),#288,.T.);
#6138=ADVANCED_FACE('',(#723),#289,.T.);
#6139=ADVANCED_FACE('',(#724),#290,.F.);
#6140=ADVANCED_FACE('',(#725),#291,.T.);
#6141=ADVANCED_FACE('',(#726),#292,.T.);
#6142=ADVANCED_FACE('',(#727),#293,.T.);
#6143=ADVANCED_FACE('',(#728,#351),#294,.T.);
#6144=ADVANCED_FACE('',(#729,#352),#295,.F.);
#6145=ADVANCED_FACE('',(#730),#395,.T.);
#6146=ADVANCED_FACE('',(#731),#396,.T.);
#6147=ADVANCED_FACE('',(#732),#397,.T.);
#6148=ADVANCED_FACE('',(#733),#398,.T.);
#6149=ADVANCED_FACE('',(#734),#399,.T.);
#6150=ADVANCED_FACE('',(#735),#400,.T.);
#6151=ADVANCED_FACE('',(#736),#401,.T.);
#6152=ADVANCED_FACE('',(#737),#402,.T.);
#6153=ADVANCED_FACE('',(#738),#403,.T.);
#6154=ADVANCED_FACE('',(#739),#404,.T.);
#6155=ADVANCED_FACE('',(#740),#405,.T.);
#6156=ADVANCED_FACE('',(#741),#406,.T.);
#6301=CLOSED_SHELL('',(#6122,#6123,#6124,#6125,#6126,#6127,#6128,#6129,
#6130,#6131,#6132,#6133,#6134,#6135,#6136,#6137,#6138,#6139,#6140,#6141,
#6142,#6143,#6144,#6145,#6146,#6147,#6148,#6149,#6150,#6151,#6152,#6153,
#6154,#6155,#6156));
#6754=AXIS2_PLACEMENT_3D('',#39801,#8060,#8061);
#6755=AXIS2_PLACEMENT_3D('',#39802,#8062,#8063);
#6756=AXIS2_PLACEMENT_3D('',#39804,#8064,#8065);
#6757=AXIS2_PLACEMENT_3D('',#39808,#8067,#8068);
#6758=AXIS2_PLACEMENT_3D('',#39809,#8069,#8070);
#6759=AXIS2_PLACEMENT_3D('',#39810,#8071,#8072);
#6760=AXIS2_PLACEMENT_3D('',#39813,#8073,#8074);
#6761=AXIS2_PLACEMENT_3D('',#39814,#8075,#8076);
#6762=AXIS2_PLACEMENT_3D('',#39816,#8078,#8079);
#6763=AXIS2_PLACEMENT_3D('',#39818,#8080,#8081);
#6764=AXIS2_PLACEMENT_3D('',#39822,#8083,#8084);
#6765=AXIS2_PLACEMENT_3D('',#39823,#8085,#8086);
#6766=AXIS2_PLACEMENT_3D('',#39824,#8087,#8088);
#6767=AXIS2_PLACEMENT_3D('',#39827,#8089,#8090);
#6768=AXIS2_PLACEMENT_3D('',#39828,#8091,#8092);
#6769=AXIS2_PLACEMENT_3D('',#39830,#8094,#8095);
#6770=AXIS2_PLACEMENT_3D('',#39832,#8096,#8097);
#6771=AXIS2_PLACEMENT_3D('',#39836,#8099,#8100);
#6772=AXIS2_PLACEMENT_3D('',#39837,#8101,#8102);
#6773=AXIS2_PLACEMENT_3D('',#39838,#8103,#8104);
#6774=AXIS2_PLACEMENT_3D('',#39841,#8105,#8106);
#6775=AXIS2_PLACEMENT_3D('',#39842,#8107,#8108);
#6776=AXIS2_PLACEMENT_3D('',#39844,#8110,#8111);
#6777=AXIS2_PLACEMENT_3D('',#39846,#8112,#8113);
#6778=AXIS2_PLACEMENT_3D('',#39850,#8115,#8116);
#6779=AXIS2_PLACEMENT_3D('',#39851,#8117,#8118);
#6780=AXIS2_PLACEMENT_3D('',#39852,#8119,#8120);
#6781=AXIS2_PLACEMENT_3D('',#39855,#8121,#8122);
#6782=AXIS2_PLACEMENT_3D('',#39857,#8124,#8125);
#6783=AXIS2_PLACEMENT_3D('',#39858,#8126,#8127);
#6784=AXIS2_PLACEMENT_3D('',#39860,#8128,#8129);
#6785=AXIS2_PLACEMENT_3D('',#39864,#8131,#8132);
#6786=AXIS2_PLACEMENT_3D('',#39865,#8133,#8134);
#6787=AXIS2_PLACEMENT_3D('',#39866,#8135,#8136);
#6788=AXIS2_PLACEMENT_3D('',#39869,#8137,#8138);
#6789=AXIS2_PLACEMENT_3D('',#39871,#8140,#8141);
#6790=AXIS2_PLACEMENT_3D('',#39872,#8142,#8143);
#6791=AXIS2_PLACEMENT_3D('',#39875,#8145,#8146);
#6792=AXIS2_PLACEMENT_3D('',#39876,#8147,#8148);
#6793=AXIS2_PLACEMENT_3D('',#39878,#8150,#8151);
#6794=AXIS2_PLACEMENT_3D('',#39880,#8153,#8154);
#6795=AXIS2_PLACEMENT_3D('',#39882,#8156,#8157);
#6796=AXIS2_PLACEMENT_3D('',#39884,#8159,#8160);
#6797=AXIS2_PLACEMENT_3D('',#39905,#8163,#8164);
#6798=AXIS2_PLACEMENT_3D('',#39923,#8166,#8167);
#6799=AXIS2_PLACEMENT_3D('',#39941,#8169,#8170);
#6800=AXIS2_PLACEMENT_3D('',#39959,#8172,#8173);
#6801=AXIS2_PLACEMENT_3D('',#39977,#8175,#8176);
#6802=AXIS2_PLACEMENT_3D('',#39992,#8177,#8178);
#6803=AXIS2_PLACEMENT_3D('',#39993,#8179,#8180);
#6804=AXIS2_PLACEMENT_3D('',#39994,#8181,#8182);
#6805=AXIS2_PLACEMENT_3D('',#39995,#8183,#8184);
#6806=AXIS2_PLACEMENT_3D('',#39996,#8185,#8186);
#6807=AXIS2_PLACEMENT_3D('',#39997,#8187,#8188);
#6808=AXIS2_PLACEMENT_3D('',#39998,#8189,#8190);
#6809=AXIS2_PLACEMENT_3D('',#39999,#8191,#8192);
#6810=AXIS2_PLACEMENT_3D('',#40000,#8193,#8194);
#6811=AXIS2_PLACEMENT_3D('',#40001,#8195,#8196);
#6812=AXIS2_PLACEMENT_3D('',#40002,#8197,#8198);
#6813=AXIS2_PLACEMENT_3D('',#40003,#8199,#8200);
#6814=AXIS2_PLACEMENT_3D('',#40004,#8201,#8202);
#6815=AXIS2_PLACEMENT_3D('',#40005,#8203,#8204);
#6816=AXIS2_PLACEMENT_3D('',#40006,#8205,#8206);
#6817=AXIS2_PLACEMENT_3D('',#40007,#8207,#8208);
#6818=AXIS2_PLACEMENT_3D('',#40008,#8209,#8210);
#6819=AXIS2_PLACEMENT_3D('',#40009,#8211,#8212);
#6820=AXIS2_PLACEMENT_3D('',#40010,#8213,#8214);
#6821=AXIS2_PLACEMENT_3D('',#40011,#8215,#8216);
#6822=AXIS2_PLACEMENT_3D('',#40012,#8217,#8218);
#6823=AXIS2_PLACEMENT_3D('',#40013,#8219,#8220);
#6824=AXIS2_PLACEMENT_3D('',#40014,#8221,#8222);
#6825=AXIS2_PLACEMENT_3D('',#40015,#8223,#8224);
#6826=AXIS2_PLACEMENT_3D('',#40016,#8225,#8226);
#6827=AXIS2_PLACEMENT_3D('',#40017,#8227,#8228);
#8060=DIRECTION('axis',(0.,0.,1.));
#8061=DIRECTION('refdir',(1.,0.,0.));
#8062=DIRECTION('center_axis',(0.,0.,1.));
#8063=DIRECTION('ref_axis',(1.,0.,0.));
#8064=DIRECTION('center_axis',(0.,0.,-1.));
#8065=DIRECTION('ref_axis',(-1.,0.,0.));
#8066=DIRECTION('',(-0.819152044288989,-1.00317192905352E-16,0.57357643635105));
#8067=DIRECTION('center_axis',(0.,0.,-1.));
#8068=DIRECTION('ref_axis',(-1.,0.,0.));
#8069=DIRECTION('center_axis',(0.,0.,-1.));
#8070=DIRECTION('ref_axis',(-1.,0.,0.));
#8071=DIRECTION('center_axis',(0.,0.,-1.));
#8072=DIRECTION('ref_axis',(-1.,0.,0.));
#8073=DIRECTION('center_axis',(0.,0.,-1.));
#8074=DIRECTION('ref_axis',(-1.,0.,0.));
#8075=DIRECTION('center_axis',(0.,0.,-1.));
#8076=DIRECTION('ref_axis',(-1.,0.,0.));
#8077=DIRECTION('',(0.819152044288998,-1.00317192905353E-16,-0.573576436351038));
#8078=DIRECTION('center_axis',(0.,0.,1.));
#8079=DIRECTION('ref_axis',(1.,0.,0.));
#8080=DIRECTION('center_axis',(0.,0.,-1.));
#8081=DIRECTION('ref_axis',(-1.,0.,0.));
#8082=DIRECTION('',(-0.819152044288989,-1.00317192905352E-16,0.57357643635105));
#8083=DIRECTION('center_axis',(0.,0.,-1.));
#8084=DIRECTION('ref_axis',(-1.,0.,0.));
#8085=DIRECTION('center_axis',(0.,0.,-1.));
#8086=DIRECTION('ref_axis',(-1.,0.,0.));
#8087=DIRECTION('center_axis',(0.,0.,-1.));
#8088=DIRECTION('ref_axis',(-1.,0.,0.));
#8089=DIRECTION('center_axis',(0.,0.,-1.));
#8090=DIRECTION('ref_axis',(-1.,0.,0.));
#8091=DIRECTION('center_axis',(0.,0.,-1.));
#8092=DIRECTION('ref_axis',(-1.,0.,0.));
#8093=DIRECTION('',(0.819152044288998,-1.00317192905353E-16,-0.573576436351038));
#8094=DIRECTION('center_axis',(0.,0.,1.));
#8095=DIRECTION('ref_axis',(1.,0.,0.));
#8096=DIRECTION('center_axis',(0.,0.,-1.));
#8097=DIRECTION('ref_axis',(-1.,0.,0.));
#8098=DIRECTION('',(-0.819152044288989,-1.00317192905352E-16,0.57357643635105));
#8099=DIRECTION('center_axis',(0.,0.,-1.));
#8100=DIRECTION('ref_axis',(-1.,0.,0.));
#8101=DIRECTION('center_axis',(0.,0.,-1.));
#8102=DIRECTION('ref_axis',(-1.,0.,0.));
#8103=DIRECTION('center_axis',(0.,0.,-1.));
#8104=DIRECTION('ref_axis',(-1.,0.,0.));
#8105=DIRECTION('center_axis',(0.,0.,-1.));
#8106=DIRECTION('ref_axis',(-1.,0.,0.));
#8107=DIRECTION('center_axis',(0.,0.,-1.));
#8108=DIRECTION('ref_axis',(-1.,0.,0.));
#8109=DIRECTION('',(0.819152044288998,-1.00317192905353E-16,-0.573576436351038));
#8110=DIRECTION('center_axis',(0.,0.,1.));
#8111=DIRECTION('ref_axis',(1.,0.,0.));
#8112=DIRECTION('center_axis',(0.,0.,-1.));
#8113=DIRECTION('ref_axis',(-1.,0.,0.));
#8114=DIRECTION('',(-0.819152044288989,-1.00317192905352E-16,0.57357643635105));
#8115=DIRECTION('center_axis',(0.,0.,-1.));
#8116=DIRECTION('ref_axis',(-1.,0.,0.));
#8117=DIRECTION('center_axis',(0.,0.,-1.));
#8118=DIRECTION('ref_axis',(-1.,0.,0.));
#8119=DIRECTION('center_axis',(0.,0.,-1.));
#8120=DIRECTION('ref_axis',(-1.,0.,0.));
#8121=DIRECTION('center_axis',(0.,0.,1.));
#8122=DIRECTION('ref_axis',(-1.,0.,0.));
#8123=DIRECTION('',(0.819152044288998,-1.00317192905353E-16,-0.573576436351038));
#8124=DIRECTION('center_axis',(0.,0.,1.));
#8125=DIRECTION('ref_axis',(-1.,0.,0.));
#8126=DIRECTION('center_axis',(0.,0.,1.));
#8127=DIRECTION('ref_axis',(1.,0.,0.));
#8128=DIRECTION('center_axis',(0.,0.,-1.));
#8129=DIRECTION('ref_axis',(1.,0.,0.));
#8130=DIRECTION('',(0.,0.,1.));
#8131=DIRECTION('center_axis',(0.,0.,1.));
#8132=DIRECTION('ref_axis',(1.,0.,0.));
#8133=DIRECTION('center_axis',(0.,0.,1.));
#8134=DIRECTION('ref_axis',(1.,0.,0.));
#8135=DIRECTION('center_axis',(0.,0.,-1.));
#8136=DIRECTION('ref_axis',(-1.,0.,0.));
#8137=DIRECTION('center_axis',(0.,0.,1.));
#8138=DIRECTION('ref_axis',(-1.,0.,0.));
#8139=DIRECTION('',(0.819152044288991,-1.00317192905352E-16,-0.573576436351047));
#8140=DIRECTION('center_axis',(0.,0.,1.));
#8141=DIRECTION('ref_axis',(-1.,0.,0.));
#8142=DIRECTION('center_axis',(0.,0.,1.));
#8143=DIRECTION('ref_axis',(1.,0.,0.));
#8144=DIRECTION('',(-0.81915204428899,-1.00317192905352E-16,0.573576436351049));
#8145=DIRECTION('center_axis',(0.,0.,1.));
#8146=DIRECTION('ref_axis',(1.,0.,0.));
#8147=DIRECTION('center_axis',(0.,0.,1.));
#8148=DIRECTION('ref_axis',(1.,0.,0.));
#8149=DIRECTION('',(0.,0.,1.));
#8150=DIRECTION('center_axis',(0.,0.,1.));
#8151=DIRECTION('ref_axis',(1.,0.,0.));
#8152=DIRECTION('',(0.,0.,1.));
#8153=DIRECTION('center_axis',(0.,0.,1.));
#8154=DIRECTION('ref_axis',(1.,0.,0.));
#8155=DIRECTION('',(0.,0.,1.));
#8156=DIRECTION('center_axis',(0.,0.,1.));
#8157=DIRECTION('ref_axis',(1.,0.,0.));
#8158=DIRECTION('',(0.,0.,1.));
#8159=DIRECTION('center_axis',(-0.500000000000003,0.866025403784437,0.));
#8160=DIRECTION('ref_axis',(-0.866025403784437,-0.500000000000003,0.));
#8161=DIRECTION('',(0.,0.,1.));
#8162=DIRECTION('',(0.,0.,1.));
#8163=DIRECTION('center_axis',(0.500000000000003,0.866025403784437,0.));
#8164=DIRECTION('ref_axis',(-0.866025403784437,0.500000000000003,0.));
#8165=DIRECTION('',(0.,0.,1.));
#8166=DIRECTION('center_axis',(-1.,0.,0.));
#8167=DIRECTION('ref_axis',(0.,0.,1.));
#8168=DIRECTION('',(0.,0.,1.));
#8169=DIRECTION('center_axis',(0.500000000000003,-0.866025403784437,0.));
#8170=DIRECTION('ref_axis',(0.866025403784437,0.500000000000003,0.));
#8171=DIRECTION('',(0.,0.,1.));
#8172=DIRECTION('center_axis',(-0.500000000000003,-0.866025403784437,0.));
#8173=DIRECTION('ref_axis',(0.866025403784437,-0.500000000000004,0.));
#8174=DIRECTION('',(0.,0.,1.));
#8175=DIRECTION('center_axis',(-1.,0.,0.));
#8176=DIRECTION('ref_axis',(0.,0.,1.));
#8177=DIRECTION('center_axis',(0.,0.,1.));
#8178=DIRECTION('ref_axis',(1.,0.,0.));
#8179=DIRECTION('center_axis',(0.,0.,1.));
#8180=DIRECTION('ref_axis',(1.,0.,0.));
#8181=DIRECTION('center_axis',(0.,0.,1.));
#8182=DIRECTION('ref_axis',(1.,0.,0.));
#8183=DIRECTION('center_axis',(0.,0.,1.));
#8184=DIRECTION('ref_axis',(1.,0.,0.));
#8185=DIRECTION('center_axis',(0.,0.,1.));
#8186=DIRECTION('ref_axis',(1.,0.,0.));
#8187=DIRECTION('center_axis',(0.,0.,1.));
#8188=DIRECTION('ref_axis',(1.,0.,0.));
#8189=DIRECTION('center_axis',(0.,0.,1.));
#8190=DIRECTION('ref_axis',(1.,0.,0.));
#8191=DIRECTION('center_axis',(0.,0.,1.));
#8192=DIRECTION('ref_axis',(1.,0.,0.));
#8193=DIRECTION('center_axis',(0.,0.,1.));
#8194=DIRECTION('ref_axis',(1.,0.,0.));
#8195=DIRECTION('center_axis',(0.,0.,-1.));
#8196=DIRECTION('ref_axis',(1.,0.,0.));
#8197=DIRECTION('center_axis',(0.,0.,-1.));
#8198=DIRECTION('ref_axis',(1.,0.,0.));
#8199=DIRECTION('center_axis',(0.,0.,-1.));
#8200=DIRECTION('ref_axis',(1.,1.77635683940025E-15,0.));
#8201=DIRECTION('center_axis',(0.,0.,-1.));
#8202=DIRECTION('ref_axis',(1.,-1.77635683940025E-15,0.));
#8203=DIRECTION('center_axis',(0.,0.,-1.));
#8204=DIRECTION('ref_axis',(1.,1.77635683940025E-15,0.));
#8205=DIRECTION('center_axis',(0.,0.,1.));
#8206=DIRECTION('ref_axis',(1.,0.,0.));
#8207=DIRECTION('center_axis',(0.,0.,1.));
#8208=DIRECTION('ref_axis',(1.,0.,0.));
#8209=DIRECTION('center_axis',(0.,0.,1.));
#8210=DIRECTION('ref_axis',(1.,0.,0.));
#8211=DIRECTION('center_axis',(0.,0.,1.));
#8212=DIRECTION('ref_axis',(1.,0.,0.));
#8213=DIRECTION('center_axis',(0.,0.,1.));
#8214=DIRECTION('ref_axis',(1.,0.,0.));
#8215=DIRECTION('center_axis',(0.,0.,1.));
#8216=DIRECTION('ref_axis',(1.,0.,0.));
#8217=DIRECTION('center_axis',(0.,0.,-1.));
#8218=DIRECTION('ref_axis',(-1.,0.,0.));
#8219=DIRECTION('center_axis',(0.,0.,-1.));
#8220=DIRECTION('ref_axis',(-1.,0.,0.));
#8221=DIRECTION('center_axis',(0.,0.,-1.));
#8222=DIRECTION('ref_axis',(-1.,0.,0.));
#8223=DIRECTION('center_axis',(0.,0.,-1.));
#8224=DIRECTION('ref_axis',(-1.,0.,0.));
#8225=DIRECTION('center_axis',(0.,0.,-1.));
#8226=DIRECTION('ref_axis',(-1.,0.,0.));
#8227=DIRECTION('center_axis',(0.,0.,-1.));
#8228=DIRECTION('ref_axis',(-1.,0.,0.));
#39801=CARTESIAN_POINT('',(0.,0.,0.));
#39802=CARTESIAN_POINT('Origin',(0.,0.,-3.52818915102791));
#39803=CARTESIAN_POINT('',(-2.5527,-3.12615588418345E-16,-3.52818915102791));
#39804=CARTESIAN_POINT('Origin',(0.,0.,-3.52818915102791));
#39805=CARTESIAN_POINT('',(-3.175,-3.88825358729285E-16,-3.09245));
#39806=CARTESIAN_POINT('',(-2.5527,-3.12615588418345E-16,-3.52818915102791));
#39807=CARTESIAN_POINT('',(3.175,3.88825358729285E-16,-3.09245));
#39808=CARTESIAN_POINT('Origin',(0.,0.,-3.09245));
#39809=CARTESIAN_POINT('Origin',(0.,0.,-3.09245));
#39810=CARTESIAN_POINT('Origin',(0.,0.,-3.09245));
#39811=CARTESIAN_POINT('',(-2.5527,3.12615588418345E-16,-2.65671084897211));
#39812=CARTESIAN_POINT('',(2.5527,-3.12615588418345E-16,-2.65671084897211));
#39813=CARTESIAN_POINT('Origin',(0.,0.,-2.65671084897211));
#39814=CARTESIAN_POINT('Origin',(0.,0.,-2.65671084897211));
#39815=CARTESIAN_POINT('',(3.175,-3.88825358729285E-16,-3.09245));
#39816=CARTESIAN_POINT('Origin',(0.,0.,-2.50583915102791));
#39817=CARTESIAN_POINT('',(-2.5527,-3.12615588418345E-16,-2.50583915102791));
#39818=CARTESIAN_POINT('Origin',(0.,0.,-2.50583915102791));
#39819=CARTESIAN_POINT('',(-3.175,-3.88825358729285E-16,-2.0701));
#39820=CARTESIAN_POINT('',(-2.5527,-3.12615588418345E-16,-2.50583915102791));
#39821=CARTESIAN_POINT('',(3.175,3.88825358729285E-16,-2.0701));
#39822=CARTESIAN_POINT('Origin',(0.,0.,-2.0701));
#39823=CARTESIAN_POINT('Origin',(0.,0.,-2.0701));
#39824=CARTESIAN_POINT('Origin',(0.,0.,-2.0701));
#39825=CARTESIAN_POINT('',(-2.5527,3.12615588418345E-16,-1.63436084897211));
#39826=CARTESIAN_POINT('',(2.5527,-3.12615588418345E-16,-1.63436084897211));
#39827=CARTESIAN_POINT('Origin',(0.,0.,-1.63436084897211));
#39828=CARTESIAN_POINT('Origin',(0.,0.,-1.63436084897211));
#39829=CARTESIAN_POINT('',(3.175,-3.88825358729285E-16,-2.0701));
#39830=CARTESIAN_POINT('Origin',(0.,0.,-1.48348915102791));
#39831=CARTESIAN_POINT('',(-2.5527,-3.12615588418345E-16,-1.48348915102791));
#39832=CARTESIAN_POINT('Origin',(0.,0.,-1.48348915102791));
#39833=CARTESIAN_POINT('',(-3.175,-3.88825358729285E-16,-1.04775));
#39834=CARTESIAN_POINT('',(-2.5527,-3.12615588418345E-16,-1.48348915102791));
#39835=CARTESIAN_POINT('',(3.175,3.88825358729285E-16,-1.04775));
#39836=CARTESIAN_POINT('Origin',(0.,0.,-1.04775));
#39837=CARTESIAN_POINT('Origin',(0.,0.,-1.04775));
#39838=CARTESIAN_POINT('Origin',(0.,0.,-1.04775));
#39839=CARTESIAN_POINT('',(-2.5527,3.12615588418345E-16,-0.612010848972106));
#39840=CARTESIAN_POINT('',(2.5527,-3.12615588418345E-16,-0.612010848972106));
#39841=CARTESIAN_POINT('Origin',(0.,0.,-0.612010848972106));
#39842=CARTESIAN_POINT('Origin',(0.,0.,-0.612010848972106));
#39843=CARTESIAN_POINT('',(3.175,-3.88825358729285E-16,-1.04775));
#39844=CARTESIAN_POINT('Origin',(0.,0.,-0.461139151027908));
#39845=CARTESIAN_POINT('',(-2.5527,-3.12615588418345E-16,-0.461139151027908));
#39846=CARTESIAN_POINT('Origin',(0.,0.,-0.461139151027908));
#39847=CARTESIAN_POINT('',(-3.175,-3.88825358729285E-16,-0.0253999999999998));
#39848=CARTESIAN_POINT('',(-2.5527,-3.12615588418345E-16,-0.461139151027908));
#39849=CARTESIAN_POINT('',(3.175,3.88825358729285E-16,-0.0254));
#39850=CARTESIAN_POINT('Origin',(0.,0.,-0.0254));
#39851=CARTESIAN_POINT('Origin',(0.,0.,-0.0254));
#39852=CARTESIAN_POINT('Origin',(0.,0.,-0.0254));
#39853=CARTESIAN_POINT('',(-3.15686252031437,3.87714758407204E-16,-0.0126999999999979));
#39854=CARTESIAN_POINT('',(3.15686252031437,-3.86604158085124E-16,-0.0126999999999974));
#39855=CARTESIAN_POINT('Origin',(0.,0.,-0.0126999999999979));
#39856=CARTESIAN_POINT('',(3.175,-3.88825358729285E-16,-0.0254));
#39857=CARTESIAN_POINT('Origin',(0.,0.,-0.0126999999999979));
#39858=CARTESIAN_POINT('Origin',(0.,0.,-25.0375057290932));
#39859=CARTESIAN_POINT('',(-3.175,-3.88825358729285E-16,-4.1402));
#39860=CARTESIAN_POINT('Origin',(0.,0.,-4.1402));
#39861=CARTESIAN_POINT('',(-3.175,-3.88825358729285E-16,-4.1148));
#39862=CARTESIAN_POINT('',(-3.175,-3.88825358729285E-16,-25.0375057290932));
#39863=CARTESIAN_POINT('',(3.175,3.88825358729285E-16,-4.1148));
#39864=CARTESIAN_POINT('Origin',(0.,0.,-4.1148));
#39865=CARTESIAN_POINT('Origin',(0.,0.,-4.1148));
#39866=CARTESIAN_POINT('Origin',(0.,0.,-4.1148));
#39867=CARTESIAN_POINT('',(-2.5527,3.12615588418345E-16,-3.6790608489721));
#39868=CARTESIAN_POINT('',(2.5527,-3.12615588418345E-16,-3.6790608489721));
#39869=CARTESIAN_POINT('Origin',(0.,0.,-3.6790608489721));
#39870=CARTESIAN_POINT('',(3.175,-3.88825358729285E-16,-4.1148));
#39871=CARTESIAN_POINT('Origin',(0.,0.,-3.6790608489721));
#39872=CARTESIAN_POINT('Origin',(0.,0.,-0.479313066130693));
#39873=CARTESIAN_POINT('',(-3.175,-3.88825358729285E-16,3.67761376907083E-15));
#39874=CARTESIAN_POINT('',(-2.49047,-3.04994611387251E-16,-0.479313066130693));
#39875=CARTESIAN_POINT('Origin',(0.,0.,3.46944695195361E-15));
#39876=CARTESIAN_POINT('Origin',(0.,0.,-4.1402));
#39877=CARTESIAN_POINT('',(-2.5527,-3.12615588418345E-16,-4.1402));
#39878=CARTESIAN_POINT('Origin',(0.,0.,-4.1402));
#39879=CARTESIAN_POINT('',(-2.5527,-3.12615588418345E-16,-4.1402));
#39880=CARTESIAN_POINT('Origin',(0.,0.,-4.1402));
#39881=CARTESIAN_POINT('',(-2.5527,-3.12615588418345E-16,-4.1402));
#39882=CARTESIAN_POINT('Origin',(0.,0.,-4.1402));
#39883=CARTESIAN_POINT('',(-2.5527,-3.12615588418345E-16,-4.1402));
#39884=CARTESIAN_POINT('Origin',(1.99537910293273E-15,6.41580486636973,
-4.1402));
#39885=CARTESIAN_POINT('',(-5.55625,3.20790243318489,-3.5052));
#39886=CARTESIAN_POINT('',(-5.55625,3.20790243318485,-0.634999999999985));
#39887=CARTESIAN_POINT('',(-5.55625,3.20790243318485,-4.1402));
#39888=CARTESIAN_POINT('',(-2.77812500000002,4.81185364977728,0.));
#39889=CARTESIAN_POINT('Ctrl Pts',(-5.55625000003183,3.20790243316647,-0.635000000013559));
#39890=CARTESIAN_POINT('Ctrl Pts',(-4.06745729956738,4.06745729954718,-1.60982338570648E-15));
#39891=CARTESIAN_POINT('Ctrl Pts',(-2.77812500000002,4.81185364977728,-1.09237954906549E-15));
#39892=CARTESIAN_POINT('',(2.60208521396521E-15,6.41580486636973,-0.635));
#39893=CARTESIAN_POINT('Ctrl Pts',(-2.77812500000002,4.81185364977728,-1.09237954906549E-15));
#39894=CARTESIAN_POINT('Ctrl Pts',(-1.48879270043265,5.55625000000739,-4.28910830115607E-16));
#39895=CARTESIAN_POINT('Ctrl Pts',(3.18280067889636E-11,6.41580486638811,
-0.635000000013576));
#39896=CARTESIAN_POINT('',(2.60208521396521E-15,6.41580486636973,-3.5052));
#39897=CARTESIAN_POINT('',(1.99537910293273E-15,6.41580486636973,-4.1402));
#39898=CARTESIAN_POINT('',(-2.77812500000002,4.81185364977728,-4.1402));
#39899=CARTESIAN_POINT('Ctrl Pts',(-2.77812500000001,4.81185364977728,-4.1402));
#39900=CARTESIAN_POINT('Ctrl Pts',(-1.48879270043264,5.55625000000739,-4.1402));
#39901=CARTESIAN_POINT('Ctrl Pts',(3.18250646004606E-11,6.4158048663881,
-3.50519999998643));
#39902=CARTESIAN_POINT('Ctrl Pts',(-5.55625000003182,3.20790243316648,-3.50519999998644));
#39903=CARTESIAN_POINT('Ctrl Pts',(-4.06745729956737,4.06745729954718,-4.1402));
#39904=CARTESIAN_POINT('Ctrl Pts',(-2.77812500000001,4.81185364977728,-4.1402));
#39905=CARTESIAN_POINT('Origin',(5.55625,3.20790243318484,-4.1402));
#39906=CARTESIAN_POINT('',(2.77812500000002,4.81185364977728,0.));
#39907=CARTESIAN_POINT('Ctrl Pts',(-3.18247703816102E-11,6.41580486638811,
-0.635000000013577));
#39908=CARTESIAN_POINT('Ctrl Pts',(1.48879270043264,5.55625000000739,-3.83026943495679E-15));
#39909=CARTESIAN_POINT('Ctrl Pts',(2.77812500000001,4.81185364977728,-2.18475909813097E-15));
#39910=CARTESIAN_POINT('',(5.55625,3.20790243318488,-0.635));
#39911=CARTESIAN_POINT('Ctrl Pts',(2.77812500000001,4.81185364977728,-2.18475909813097E-15));
#39912=CARTESIAN_POINT('Ctrl Pts',(4.06745729956737,4.06745729954718,-5.70175753880392E-16));
#39913=CARTESIAN_POINT('Ctrl Pts',(5.55625000003182,3.20790243316648,-0.635000000013555));
#39914=CARTESIAN_POINT('',(5.55625,3.20790243318488,-3.5052));
#39915=CARTESIAN_POINT('',(5.55625,3.20790243318484,-4.1402));
#39916=CARTESIAN_POINT('',(2.77812500000002,4.81185364977728,-4.1402));
#39917=CARTESIAN_POINT('Ctrl Pts',(2.77812500000002,4.81185364977728,-4.1402));
#39918=CARTESIAN_POINT('Ctrl Pts',(4.06745729956737,4.06745729954718,-4.1402));
#39919=CARTESIAN_POINT('Ctrl Pts',(5.55625000003181,3.20790243316648,-3.50519999998645));
#39920=CARTESIAN_POINT('Ctrl Pts',(-3.18250646004606E-11,6.4158048663881,
-3.50519999998643));
#39921=CARTESIAN_POINT('Ctrl Pts',(1.48879270043265,5.55625000000739,-4.1402));
#39922=CARTESIAN_POINT('Ctrl Pts',(2.77812500000002,4.81185364977728,-4.1402));
#39923=CARTESIAN_POINT('Origin',(5.55625,3.20790243318484,-4.1402));
#39924=CARTESIAN_POINT('',(5.55625,-3.20790243318489,-0.635));
#39925=CARTESIAN_POINT('',(5.55625,0.,0.));
#39926=CARTESIAN_POINT('Ctrl Pts',(5.55625,-3.20790243322164,-0.635000000013576));
#39927=CARTESIAN_POINT('Ctrl Pts',(5.55625,-1.48879270046021,-1.77635683940025E-15));
#39928=CARTESIAN_POINT('Ctrl Pts',(5.55625,-1.09237954906549E-15,-1.63856932359823E-15));
#39929=CARTESIAN_POINT('',(5.55625,-3.20790243318489,-3.5052));
#39930=CARTESIAN_POINT('',(5.55625,-3.20790243318489,-4.1402));
#39931=CARTESIAN_POINT('',(5.55625,0.,-4.1402));
#39932=CARTESIAN_POINT('Ctrl Pts',(5.55625,-3.20790243322163,-3.50519999998643));
#39933=CARTESIAN_POINT('Ctrl Pts',(5.55625,-1.4887927004602,-4.1402));
#39934=CARTESIAN_POINT('Ctrl Pts',(5.55625,7.64665684345841E-15,-4.1402));
#39935=CARTESIAN_POINT('Ctrl Pts',(5.55625,7.64665684345841E-15,-4.1402));
#39936=CARTESIAN_POINT('Ctrl Pts',(5.55625,1.48879270046021,-4.1402));
#39937=CARTESIAN_POINT('Ctrl Pts',(5.55625,3.20790243322163,-3.50519999998643));
#39938=CARTESIAN_POINT('Ctrl Pts',(5.55625,-1.09237954906549E-15,-1.63856932359823E-15));
#39939=CARTESIAN_POINT('Ctrl Pts',(5.55625,1.4887927004602,-1.41042199544234E-15));
#39940=CARTESIAN_POINT('Ctrl Pts',(5.55625,3.20790243322162,-0.635000000013571));
#39941=CARTESIAN_POINT('Origin',(7.33180410152027E-16,-6.41580486636977,
-4.1402));
#39942=CARTESIAN_POINT('',(2.77812500000002,-4.81185364977728,0.));
#39943=CARTESIAN_POINT('Ctrl Pts',(5.55625000003183,-3.20790243316651,-0.635000000013574));
#39944=CARTESIAN_POINT('Ctrl Pts',(4.06745729956739,-4.06745729954721,-2.75335310107039E-14));
#39945=CARTESIAN_POINT('Ctrl Pts',(2.77812500000003,-4.81185364977731,-2.78556785011701E-14));
#39946=CARTESIAN_POINT('',(-7.06899816460549E-14,-6.41580486636973,-0.635));
#39947=CARTESIAN_POINT('Ctrl Pts',(2.77812500000003,-4.81185364977731,-2.78556785011701E-14));
#39948=CARTESIAN_POINT('Ctrl Pts',(1.48879270043264,-5.55625000000743,-2.85795084241335E-14));
#39949=CARTESIAN_POINT('Ctrl Pts',(-3.18624303944503E-11,-6.41580486638817,
-0.63500000001362));
#39950=CARTESIAN_POINT('',(-7.06899816460549E-14,-6.41580486636973,-3.5052));
#39951=CARTESIAN_POINT('',(7.33180410152027E-16,-6.41580486636977,-4.1402));
#39952=CARTESIAN_POINT('',(2.77812500000002,-4.81185364977728,-4.1402));
#39953=CARTESIAN_POINT('Ctrl Pts',(2.77812500000004,-4.81185364977731,-4.14019999999997));
#39954=CARTESIAN_POINT('Ctrl Pts',(1.48879270043264,-5.55625000000743,-4.14019999999997));
#39955=CARTESIAN_POINT('Ctrl Pts',(-3.18500732027373E-11,-6.41580486638816,
-3.50519999998639));
#39956=CARTESIAN_POINT('Ctrl Pts',(5.55625000003182,-3.20790243316652,-3.50519999998643));
#39957=CARTESIAN_POINT('Ctrl Pts',(4.06745729956738,-4.06745729954721,-4.14019999999997));
#39958=CARTESIAN_POINT('Ctrl Pts',(2.77812500000004,-4.81185364977731,-4.14019999999997));
#39959=CARTESIAN_POINT('Origin',(-5.55625,-3.20790243318488,-4.1402));
#39960=CARTESIAN_POINT('',(-2.77812500000002,-4.81185364977727,0.));
#39961=CARTESIAN_POINT('Ctrl Pts',(3.17573942648891E-11,-6.41580486638811,
-0.635000000013576));
#39962=CARTESIAN_POINT('Ctrl Pts',(-1.48879270043268,-5.5562500000074,-2.71449529520851E-14));
#39963=CARTESIAN_POINT('Ctrl Pts',(-2.77812500000004,-4.81185364977731,
-2.68998463957378E-14));
#39964=CARTESIAN_POINT('',(-5.55625,-3.20790243318489,-0.635));
#39965=CARTESIAN_POINT('Ctrl Pts',(-2.77812500000004,-4.81185364977731,
-2.68998463957378E-14));
#39966=CARTESIAN_POINT('Ctrl Pts',(-4.06745729956739,-4.06745729954721,
-2.66940704394404E-14));
#39967=CARTESIAN_POINT('Ctrl Pts',(-5.55625000003183,-3.20790243316651,
-0.635000000013575));
#39968=CARTESIAN_POINT('',(-5.55625,-3.20790243318489,-3.5052));
#39969=CARTESIAN_POINT('',(-5.55625,-3.20790243318488,-4.1402));
#39970=CARTESIAN_POINT('',(-2.77812500000002,-4.81185364977727,-4.1402));
#39971=CARTESIAN_POINT('Ctrl Pts',(-2.77812500000003,-4.81185364977731,
-4.14019999999998));
#39972=CARTESIAN_POINT('Ctrl Pts',(-4.06745729956739,-4.06745729954721,
-4.14019999999998));
#39973=CARTESIAN_POINT('Ctrl Pts',(-5.55625000003182,-3.20790243316651,
-3.50519999998643));
#39974=CARTESIAN_POINT('Ctrl Pts',(3.17612191099431E-11,-6.41580486638811,
-3.50519999998642));
#39975=CARTESIAN_POINT('Ctrl Pts',(-1.48879270043268,-5.55625000000741,
-4.14019999999997));
#39976=CARTESIAN_POINT('Ctrl Pts',(-2.77812500000003,-4.81185364977731,
-4.14019999999998));
#39977=CARTESIAN_POINT('Origin',(-5.55625,3.20790243318485,-4.1402));
#39978=CARTESIAN_POINT('',(-5.55625,0.,0.));
#39979=CARTESIAN_POINT('Ctrl Pts',(-5.55625,-3.20790243322164,-0.635000000013575));
#39980=CARTESIAN_POINT('Ctrl Pts',(-5.55625,-1.48879270046021,-1.0547118733939E-15));
#39981=CARTESIAN_POINT('Ctrl Pts',(-5.55625,-3.82332842172921E-15,-2.73094887266373E-16));
#39982=CARTESIAN_POINT('Ctrl Pts',(-5.55625,-3.82332842172921E-15,-2.73094887266373E-16));
#39983=CARTESIAN_POINT('Ctrl Pts',(-5.55625,1.48879270046019,3.24241151997365E-16));
#39984=CARTESIAN_POINT('Ctrl Pts',(-5.55625,3.2079024332216,-0.63500000001356));
#39985=CARTESIAN_POINT('',(-5.55625,0.,-4.1402));
#39986=CARTESIAN_POINT('Ctrl Pts',(-5.55625,2.73094887266372E-15,-4.1402));
#39987=CARTESIAN_POINT('Ctrl Pts',(-5.55625,1.48879270046021,-4.1402));
#39988=CARTESIAN_POINT('Ctrl Pts',(-5.55625,3.20790243322164,-3.50519999998643));
#39989=CARTESIAN_POINT('Ctrl Pts',(-5.55625,-3.20790243322165,-3.50519999998642));
#39990=CARTESIAN_POINT('Ctrl Pts',(-5.55625,-1.48879270046021,-4.1402));
#39991=CARTESIAN_POINT('Ctrl Pts',(-5.55625,2.73094887266372E-15,-4.1402));
#39992=CARTESIAN_POINT('Origin',(-11.1125,-1.43114686768087E-14,0.));
#39993=CARTESIAN_POINT('Origin',(0.,0.,0.));
#39994=CARTESIAN_POINT('Origin',(0.,0.,0.));
#39995=CARTESIAN_POINT('Origin',(0.,0.,0.));
#39996=CARTESIAN_POINT('Origin',(0.,0.,0.));
#39997=CARTESIAN_POINT('Origin',(0.,0.,0.));
#39998=CARTESIAN_POINT('Origin',(0.,0.,0.));
#39999=CARTESIAN_POINT('Origin',(-11.1125,-1.43114686768087E-14,-4.1402));
#40000=CARTESIAN_POINT('Origin',(0.,0.,-4.1402));
#40001=CARTESIAN_POINT('Origin',(0.,0.,-4.1402));
#40002=CARTESIAN_POINT('Origin',(0.,0.,-4.1402));
#40003=CARTESIAN_POINT('Origin',(0.,0.,-4.1402));
#40004=CARTESIAN_POINT('Origin',(0.,0.,-4.1402));
#40005=CARTESIAN_POINT('Origin',(0.,0.,-4.1402));
#40006=CARTESIAN_POINT('Origin',(0.,0.,-4.1402));
#40007=CARTESIAN_POINT('Origin',(0.,0.,-4.1402));
#40008=CARTESIAN_POINT('Origin',(0.,0.,-4.1402));
#40009=CARTESIAN_POINT('Origin',(0.,0.,-4.1402));
#40010=CARTESIAN_POINT('Origin',(0.,0.,-4.1402));
#40011=CARTESIAN_POINT('Origin',(0.,0.,-4.1402));
#40012=CARTESIAN_POINT('Origin',(0.,0.,0.));
#40013=CARTESIAN_POINT('Origin',(0.,0.,0.));
#40014=CARTESIAN_POINT('Origin',(0.,0.,0.));
#40015=CARTESIAN_POINT('Origin',(0.,0.,0.));
#40016=CARTESIAN_POINT('Origin',(0.,0.,0.));
#40017=CARTESIAN_POINT('Origin',(0.,0.,0.));
#40794=UNCERTAINTY_MEASURE_WITH_UNIT(LENGTH_MEASURE(0.01),#40810,
'DISTANCE_ACCURACY_VALUE',
'Maximum model space distance between geometric entities at asserted c
onnectivities');
#40799=UNCERTAINTY_MEASURE_WITH_UNIT(LENGTH_MEASURE(0.01),#40810,
'DISTANCE_ACCURACY_VALUE',
'Maximum model space distance between geometric entities at asserted c
onnectivities');
#40804=(
GEOMETRIC_REPRESENTATION_CONTEXT(3)
GLOBAL_UNCERTAINTY_ASSIGNED_CONTEXT((#40794))
GLOBAL_UNIT_ASSIGNED_CONTEXT((#40810,#40812,#40813))
REPRESENTATION_CONTEXT('','3D')
);
#40809=(
GEOMETRIC_REPRESENTATION_CONTEXT(3)
GLOBAL_UNCERTAINTY_ASSIGNED_CONTEXT((#40799))
GLOBAL_UNIT_ASSIGNED_CONTEXT((#40810,#40812,#40813))
REPRESENTATION_CONTEXT('','3D')
);
#40810=(
LENGTH_UNIT()
NAMED_UNIT(*)
SI_UNIT(.MILLI.,.METRE.)
);
#40812=(
NAMED_UNIT(*)
PLANE_ANGLE_UNIT()
SI_UNIT($,.RADIAN.)
);
#40813=(
NAMED_UNIT(*)
SI_UNIT($,.STERADIAN.)
SOLID_ANGLE_UNIT()
);
#40818=SHAPE_DEFINITION_REPRESENTATION(#40827,#40860);
#40827=PRODUCT_DEFINITION_SHAPE('',$,#40870);
#40860=SHAPE_REPRESENTATION('',(#6754),#40804);
#40865=PRODUCT_DEFINITION_CONTEXT('part definition',#40894,'design');
#40870=PRODUCT_DEFINITION('Hex Jam Nut 0.2500-20-D-S',
'Hex Jam Nut 0.2500-20-D-S',#40879,#40865);
#40879=PRODUCT_DEFINITION_FORMATION('',$,#40900);
#40894=APPLICATION_CONTEXT(
'Core Data for Automotive Mechanical Design Process');
#40895=PRODUCT_CONTEXT('part definition',#40894,'mechanical');
#40900=PRODUCT('Hex Jam Nut 0.2500-20-D-S','Hex Jam Nut 0.2500-20-D-S',
$,(#40895));
#40909=PRESENTATION_STYLE_ASSIGNMENT((#40914));
#40914=SURFACE_STYLE_USAGE(.BOTH.,#40919);
#40919=SURFACE_SIDE_STYLE('',(#40924));
#40924=SURFACE_STYLE_FILL_AREA(#40929);
#40929=FILL_AREA_STYLE('Opaque(31,36,43)',(#40934));
#40934=FILL_AREA_STYLE_COLOUR('Opaque(31,36,43)',#40939);
#40939=COLOUR_RGB('Opaque(31,36,43)',0.12156862745098,0.141176470588235,
0.168627450980392);
ENDSEC;
END-ISO-10303-21;
